ISO-10303-21;
HEADER;
/* Generated by software containing ST-Developer
 * from STEP Tools, Inc. (www.steptools.com) 
 */

FILE_DESCRIPTION(
/* description */ ('Four-bar parallelogram arm'),
/* implementation_level */ '2;1');

FILE_NAME(
/* name */ 'Front spacer (1).step',
/* time_stamp */ '2026-10-28T03:24:55-07:00',
/* author */ (''),
/* organization */ (''),
/* preprocessor_version */ 'ST-DEVELOPER v20.2',
/* originating_system */ 'Autodesk Translation Framework v15.17.0.0',
/* authorisation */ '');

FILE_SCHEMA (('AUTOMOTIVE_DESIGN { 1 0 10303 214 3 1 1 }'));
ENDSEC;

DATA;
#10=MECHANICAL_DESIGN_GEOMETRIC_PRESENTATION_REPRESENTATION('',(#672),#14512);
#564=SHAPE_REPRESENTATION_RELATIONSHIP('SRR','None',#14789,#614);
#614=ADVANCED_BREP_SHAPE_REPRESENTATION('',(#728),#14504);
#672=STYLED_ITEM('',(#15080),#728);
#728=MANIFOLD_SOLID_BREP('Body1',#7378);
#984=FACE_BOUND('',#2240,.T.);
#985=FACE_BOUND('',#2242,.T.);
#1173=PLANE('',#8818);
#1174=PLANE('',#8819);
#1568=FACE_OUTER_BOUND('',#2237,.T.);
#1569=FACE_OUTER_BOUND('',#2238,.T.);
#1570=FACE_OUTER_BOUND('',#2239,.T.);
#1571=FACE_OUTER_BOUND('',#2241,.T.);
#2237=EDGE_LOOP('',(#6536,#6537,#6538,#6539));
#2238=EDGE_LOOP('',(#6540,#6541,#6542,#6543));
#2239=EDGE_LOOP('',(#6544));
#2240=EDGE_LOOP('',(#6545));
#2241=EDGE_LOOP('',(#6546));
#2242=EDGE_LOOP('',(#6547));
#2663=LINE('',#14144,#3057);
#2664=LINE('',#14150,#3058);
#3057=VECTOR('',#11073,0.504999999999999);
#3058=VECTOR('',#11080,0.699999999999999);
#3499=CIRCLE('',#8813,0.504999999999999);
#3500=CIRCLE('',#8814,0.504999999999999);
#3501=CIRCLE('',#8816,0.699999999999999);
#3502=CIRCLE('',#8817,0.699999999999999);
#4067=VERTEX_POINT('',#14141);
#4068=VERTEX_POINT('',#14143);
#4069=VERTEX_POINT('',#14147);
#4070=VERTEX_POINT('',#14149);
#4899=EDGE_CURVE('',#4067,#4067,#3499,.T.);
#4900=EDGE_CURVE('',#4067,#4068,#2663,.T.);
#4901=EDGE_CURVE('',#4068,#4068,#3500,.T.);
#4902=EDGE_CURVE('',#4069,#4069,#3501,.T.);
#4903=EDGE_CURVE('',#4069,#4070,#2664,.T.);
#4904=EDGE_CURVE('',#4070,#4070,#3502,.T.);
#6536=ORIENTED_EDGE('',*,*,#4899,.F.);
#6537=ORIENTED_EDGE('',*,*,#4900,.T.);
#6538=ORIENTED_EDGE('',*,*,#4901,.T.);
#6539=ORIENTED_EDGE('',*,*,#4900,.F.);
#6540=ORIENTED_EDGE('',*,*,#4902,.F.);
#6541=ORIENTED_EDGE('',*,*,#4903,.T.);
#6542=ORIENTED_EDGE('',*,*,#4904,.T.);
#6543=ORIENTED_EDGE('',*,*,#4903,.F.);
#6544=ORIENTED_EDGE('',*,*,#4902,.T.);
#6545=ORIENTED_EDGE('',*,*,#4899,.T.);
#6546=ORIENTED_EDGE('',*,*,#4904,.F.);
#6547=ORIENTED_EDGE('',*,*,#4901,.F.);
#6885=CYLINDRICAL_SURFACE('',#8812,0.504999999999999);
#6886=CYLINDRICAL_SURFACE('',#8815,0.699999999999999);
#7273=ADVANCED_FACE('',(#1568),#6885,.F.);
#7274=ADVANCED_FACE('',(#1569),#6886,.T.);
#7275=ADVANCED_FACE('',(#1570,#984),#1173,.T.);
#7276=ADVANCED_FACE('',(#1571,#985),#1174,.F.);
#7378=CLOSED_SHELL('',(#7273,#7274,#7275,#7276));
#8811=AXIS2_PLACEMENT_3D('',#14139,#11067,#11068);
#8812=AXIS2_PLACEMENT_3D('',#14140,#11069,#11070);
#8813=AXIS2_PLACEMENT_3D('',#14142,#11071,#11072);
#8814=AXIS2_PLACEMENT_3D('',#14145,#11074,#11075);
#8815=AXIS2_PLACEMENT_3D('',#14146,#11076,#11077);
#8816=AXIS2_PLACEMENT_3D('',#14148,#11078,#11079);
#8817=AXIS2_PLACEMENT_3D('',#14151,#11081,#11082);
#8818=AXIS2_PLACEMENT_3D('',#14152,#11083,#11084);
#8819=AXIS2_PLACEMENT_3D('',#14153,#11085,#11086);
#11067=DIRECTION('axis',(0.,0.,1.));
#11068=DIRECTION('refdir',(1.,0.,0.));
#11069=DIRECTION('center_axis',(0.,1.,0.));
#11070=DIRECTION('ref_axis',(1.,0.,0.));
#11071=DIRECTION('center_axis',(0.,-1.,0.));
#11072=DIRECTION('ref_axis',(1.,0.,0.));
#11073=DIRECTION('',(0.,-1.,0.));
#11074=DIRECTION('center_axis',(0.,-1.,0.));
#11075=DIRECTION('ref_axis',(1.,0.,0.));
#11076=DIRECTION('center_axis',(0.,1.,0.));
#11077=DIRECTION('ref_axis',(1.,0.,0.));
#11078=DIRECTION('center_axis',(0.,1.,0.));
#11079=DIRECTION('ref_axis',(1.,0.,0.));
#11080=DIRECTION('',(0.,-1.,0.));
#11081=DIRECTION('center_axis',(0.,1.,0.));
#11082=DIRECTION('ref_axis',(1.,0.,0.));
#11083=DIRECTION('center_axis',(0.,1.,0.));
#11084=DIRECTION('ref_axis',(1.,0.,0.));
#11085=DIRECTION('center_axis',(0.,1.,0.));
#11086=DIRECTION('ref_axis',(1.,0.,0.));
#14139=CARTESIAN_POINT('',(0.,0.,0.));
#14140=CARTESIAN_POINT('Origin',(20.,-1.6,8.));
#14141=CARTESIAN_POINT('',(19.495,-1.05,8.));
#14142=CARTESIAN_POINT('Origin',(20.,-1.05,8.));
#14143=CARTESIAN_POINT('',(19.495,-1.6,8.));
#14144=CARTESIAN_POINT('',(19.495,-1.6,8.));
#14145=CARTESIAN_POINT('Origin',(20.,-1.6,8.));
#14146=CARTESIAN_POINT('Origin',(20.,-1.6,8.));
#14147=CARTESIAN_POINT('',(19.3,-1.05,8.));
#14148=CARTESIAN_POINT('Origin',(20.,-1.05,8.));
#14149=CARTESIAN_POINT('',(19.3,-1.6,8.));
#14150=CARTESIAN_POINT('',(19.3,-1.6,8.));
#14151=CARTESIAN_POINT('Origin',(20.,-1.6,8.));
#14152=CARTESIAN_POINT('Origin',(20.,-1.05,8.));
#14153=CARTESIAN_POINT('Origin',(20.,-1.6,8.));
#14447=UNCERTAINTY_MEASURE_WITH_UNIT(LENGTH_MEASURE(0.001),#14513,
'DISTANCE_ACCURACY_VALUE',
'Maximum model space distance between geometric entities at asserted c
onnectivities');
#14455=UNCERTAINTY_MEASURE_WITH_UNIT(LENGTH_MEASURE(0.001),#14513,
'DISTANCE_ACCURACY_VALUE',
'Maximum model space distance between geometric entities at asserted c
onnectivities');
#14504=(
GEOMETRIC_REPRESENTATION_CONTEXT(3)
GLOBAL_UNCERTAINTY_ASSIGNED_CONTEXT((#14447))
GLOBAL_UNIT_ASSIGNED_CONTEXT((#14513,#14515,#14516))
REPRESENTATION_CONTEXT('','3D')
);
#14512=(
GEOMETRIC_REPRESENTATION_CONTEXT(3)
GLOBAL_UNCERTAINTY_ASSIGNED_CONTEXT((#14455))
GLOBAL_UNIT_ASSIGNED_CONTEXT((#14513,#14515,#14516))
REPRESENTATION_CONTEXT('','3D')
);
#14513=(
LENGTH_UNIT()
NAMED_UNIT(*)
SI_UNIT(.CENTI.,.METRE.)
);
#14515=(
NAMED_UNIT(*)
PLANE_ANGLE_UNIT()
SI_UNIT($,.RADIAN.)
);
#14516=(
NAMED_UNIT(*)
SI_UNIT($,.STERADIAN.)
SOLID_ANGLE_UNIT()
);
#14565=SHAPE_DEFINITION_REPRESENTATION(#14681,#14789);
#14681=PRODUCT_DEFINITION_SHAPE('',$,#14846);
#14789=SHAPE_REPRESENTATION('',(#8811),#14504);
#14797=PRODUCT_DEFINITION_CONTEXT('part definition',#14967,'design');
#14846=PRODUCT_DEFINITION('Front spacer (1)','Front spacer (1)',#14902,#14797);
#14902=PRODUCT_DEFINITION_FORMATION('',$,#15017);
#14967=APPLICATION_CONTEXT(
'Core Data for Automotive Mechanical Design Process');
#14968=PRODUCT_CONTEXT('part definition',#14967,'mechanical');
#15017=PRODUCT('Front spacer (1)','Front spacer (1)','Front spacer (1)',(#14968));
#15074=COLOUR_RGB('Sky Blue',0.24,0.69,0.87);
#15075=FILL_AREA_STYLE_COLOUR('',#15074);
#15076=FILL_AREA_STYLE('',(#15075));
#15077=SURFACE_STYLE_FILL_AREA(#15076);
#15078=SURFACE_SIDE_STYLE('',(#15077));
#15079=SURFACE_STYLE_USAGE(.BOTH.,#15078);
#15080=PRESENTATION_STYLE_ASSIGNMENT((#15079));
ENDSEC;
END-ISO-10303-21;
